ISO-10303-21;
HEADER;
/* Generated by software containing ST-Developer
 * from STEP Tools, Inc. (www.steptools.com) 
 */

FILE_DESCRIPTION(
/* description */ ('STEP AP214'),
/* implementation_level */ '2;1');

FILE_NAME(
/* name */ 'Socket Head Cap Screw M6x20.step',
/* time_stamp */ '2026-11-15T14:49:54-08:00',
/* author */ (''),
/* organization */ (''),
/* preprocessor_version */ 'ST-DEVELOPER v20.2',
/* originating_system */ 'Autodesk Translation Framework v15.17.0.0',
/* authorisation */ '');

FILE_SCHEMA (('AUTOMOTIVE_DESIGN { 1 0 10303 214 3 1 1 }'));
ENDSEC;

DATA;
#10=MECHANICAL_DESIGN_GEOMETRIC_PRESENTATION_REPRESENTATION('',(#1127),#66721);
#576=CONICAL_SURFACE('',#28568,5.,0.785398163397445);
#577=CONICAL_SURFACE('',#28570,2.4585,0.785398163397448);
#1063=SHAPE_REPRESENTATION_RELATIONSHIP('SRR','None',#66926,#1094);
#1094=ADVANCED_BREP_SHAPE_REPRESENTATION('',(#1162),#66717);
#1127=STYLED_ITEM('',(#67095),#1162);
#1162=MANIFOLD_SOLID_BREP('Body1',#25693);
#1469=FACE_BOUND('',#5383,.T.);
#1470=FACE_BOUND('',#5385,.T.);
#2219=PLANE('',#28576);
#2220=PLANE('',#28577);
#2221=PLANE('',#28578);
#2222=PLANE('',#28579);
#2223=PLANE('',#28580);
#2224=PLANE('',#28581);
#2225=PLANE('',#28582);
#2226=PLANE('',#28583);
#2227=PLANE('',#28584);
#2228=PLANE('',#28585);
#3634=FACE_OUTER_BOUND('',#5377,.T.);
#3635=FACE_OUTER_BOUND('',#5378,.T.);
#3636=FACE_OUTER_BOUND('',#5379,.T.);
#3637=FACE_OUTER_BOUND('',#5380,.T.);
#3638=FACE_OUTER_BOUND('',#5381,.T.);
#3639=FACE_OUTER_BOUND('',#5382,.T.);
#3640=FACE_OUTER_BOUND('',#5384,.T.);
#3641=FACE_OUTER_BOUND('',#5386,.T.);
#3642=FACE_OUTER_BOUND('',#5387,.T.);
#3643=FACE_OUTER_BOUND('',#5388,.T.);
#3644=FACE_OUTER_BOUND('',#5389,.T.);
#3645=FACE_OUTER_BOUND('',#5390,.T.);
#3646=FACE_OUTER_BOUND('',#5391,.T.);
#3647=FACE_OUTER_BOUND('',#5392,.T.);
#5377=EDGE_LOOP('',(#23466,#23467,#23468,#23469));
#5378=EDGE_LOOP('',(#23470,#23471,#23472,#23473));
#5379=EDGE_LOOP('',(#23474,#23475,#23476,#23477,#23478));
#5380=EDGE_LOOP('',(#23479,#23480,#23481,#23482,#23483));
#5381=EDGE_LOOP('',(#23484));
#5382=EDGE_LOOP('',(#23485));
#5383=EDGE_LOOP('',(#23486,#23487,#23488,#23489,#23490,#23491));
#5384=EDGE_LOOP('',(#23492));
#5385=EDGE_LOOP('',(#23493));
#5386=EDGE_LOOP('',(#23494,#23495,#23496,#23497));
#5387=EDGE_LOOP('',(#23498,#23499,#23500,#23501));
#5388=EDGE_LOOP('',(#23502,#23503,#23504,#23505));
#5389=EDGE_LOOP('',(#23506,#23507,#23508,#23509));
#5390=EDGE_LOOP('',(#23510,#23511,#23512,#23513));
#5391=EDGE_LOOP('',(#23514,#23515,#23516,#23517));
#5392=EDGE_LOOP('',(#23518,#23519,#23520,#23521,#23522,#23523));
#7361=LINE('',#66232,#9350);
#7362=LINE('',#66236,#9351);
#7363=LINE('',#66243,#9352);
#7364=LINE('',#66248,#9353);
#7365=LINE('',#66254,#9354);
#7366=LINE('',#66256,#9355);
#7367=LINE('',#66258,#9356);
#7368=LINE('',#66260,#9357);
#7369=LINE('',#66262,#9358);
#7370=LINE('',#66263,#9359);
#7371=LINE('',#66267,#9360);
#7372=LINE('',#66269,#9361);
#7373=LINE('',#66270,#9362);
#7374=LINE('',#66273,#9363);
#7375=LINE('',#66274,#9364);
#7376=LINE('',#66277,#9365);
#7377=LINE('',#66278,#9366);
#7378=LINE('',#66281,#9367);
#7379=LINE('',#66282,#9368);
#7380=LINE('',#66285,#9369);
#7381=LINE('',#66286,#9370);
#7382=LINE('',#66288,#9371);
#9350=VECTOR('',#35686,5.);
#9351=VECTOR('',#35691,5.);
#9352=VECTOR('',#35698,2.4585);
#9353=VECTOR('',#35705,3.);
#9354=VECTOR('',#35712,1000.);
#9355=VECTOR('',#35713,1000.);
#9356=VECTOR('',#35714,1000.);
#9357=VECTOR('',#35715,1000.);
#9358=VECTOR('',#35716,1000.);
#9359=VECTOR('',#35717,1000.);
#9360=VECTOR('',#35722,1000.);
#9361=VECTOR('',#35723,1000.);
#9362=VECTOR('',#35724,1000.);
#9363=VECTOR('',#35727,1000.);
#9364=VECTOR('',#35728,1000.);
#9365=VECTOR('',#35731,1000.);
#9366=VECTOR('',#35732,1000.);
#9367=VECTOR('',#35735,1000.);
#9368=VECTOR('',#35736,1000.);
#9369=VECTOR('',#35739,1000.);
#9370=VECTOR('',#35740,1000.);
#9371=VECTOR('',#35743,1000.);
#10581=CIRCLE('',#28566,5.);
#10582=CIRCLE('',#28567,5.);
#10583=CIRCLE('',#28569,4.4);
#10584=CIRCLE('',#28571,3.);
#10585=CIRCLE('',#28572,2.4585);
#10586=CIRCLE('',#28573,3.);
#10587=CIRCLE('',#28575,3.);
#12880=VERTEX_POINT('',#66229);
#12881=VERTEX_POINT('',#66231);
#12882=VERTEX_POINT('',#66235);
#12883=VERTEX_POINT('',#66239);
#12884=VERTEX_POINT('',#66240);
#12885=VERTEX_POINT('',#66242);
#12886=VERTEX_POINT('',#66247);
#12887=VERTEX_POINT('',#66252);
#12888=VERTEX_POINT('',#66253);
#12889=VERTEX_POINT('',#66255);
#12890=VERTEX_POINT('',#66257);
#12891=VERTEX_POINT('',#66259);
#12892=VERTEX_POINT('',#66261);
#12893=VERTEX_POINT('',#66266);
#12894=VERTEX_POINT('',#66268);
#12895=VERTEX_POINT('',#66272);
#12896=VERTEX_POINT('',#66276);
#12897=VERTEX_POINT('',#66280);
#12898=VERTEX_POINT('',#66284);
#16426=EDGE_CURVE('',#12880,#12880,#10581,.T.);
#16427=EDGE_CURVE('',#12880,#12881,#7361,.T.);
#16428=EDGE_CURVE('',#12881,#12881,#10582,.T.);
#16429=EDGE_CURVE('',#12881,#12882,#7362,.T.);
#16430=EDGE_CURVE('',#12882,#12882,#10583,.T.);
#16431=EDGE_CURVE('',#12883,#12884,#10584,.T.);
#16432=EDGE_CURVE('',#12884,#12885,#7363,.T.);
#16433=EDGE_CURVE('',#12885,#12885,#10585,.T.);
#16434=EDGE_CURVE('',#12884,#12883,#10586,.T.);
#16435=EDGE_CURVE('',#12883,#12886,#7364,.T.);
#16436=EDGE_CURVE('',#12886,#12886,#10587,.T.);
#16437=EDGE_CURVE('',#12887,#12888,#7365,.T.);
#16438=EDGE_CURVE('',#12889,#12887,#7366,.T.);
#16439=EDGE_CURVE('',#12890,#12889,#7367,.T.);
#16440=EDGE_CURVE('',#12891,#12890,#7368,.T.);
#16441=EDGE_CURVE('',#12892,#12891,#7369,.T.);
#16442=EDGE_CURVE('',#12888,#12892,#7370,.T.);
#16443=EDGE_CURVE('',#12893,#12888,#7371,.T.);
#16444=EDGE_CURVE('',#12894,#12893,#7372,.T.);
#16445=EDGE_CURVE('',#12894,#12887,#7373,.T.);
#16446=EDGE_CURVE('',#12895,#12894,#7374,.T.);
#16447=EDGE_CURVE('',#12895,#12889,#7375,.T.);
#16448=EDGE_CURVE('',#12896,#12895,#7376,.T.);
#16449=EDGE_CURVE('',#12896,#12890,#7377,.T.);
#16450=EDGE_CURVE('',#12897,#12896,#7378,.T.);
#16451=EDGE_CURVE('',#12897,#12891,#7379,.T.);
#16452=EDGE_CURVE('',#12898,#12897,#7380,.T.);
#16453=EDGE_CURVE('',#12898,#12892,#7381,.T.);
#16454=EDGE_CURVE('',#12893,#12898,#7382,.T.);
#23466=ORIENTED_EDGE('',*,*,#16426,.F.);
#23467=ORIENTED_EDGE('',*,*,#16427,.T.);
#23468=ORIENTED_EDGE('',*,*,#16428,.T.);
#23469=ORIENTED_EDGE('',*,*,#16427,.F.);
#23470=ORIENTED_EDGE('',*,*,#16428,.F.);
#23471=ORIENTED_EDGE('',*,*,#16429,.T.);
#23472=ORIENTED_EDGE('',*,*,#16430,.T.);
#23473=ORIENTED_EDGE('',*,*,#16429,.F.);
#23474=ORIENTED_EDGE('',*,*,#16431,.T.);
#23475=ORIENTED_EDGE('',*,*,#16432,.T.);
#23476=ORIENTED_EDGE('',*,*,#16433,.F.);
#23477=ORIENTED_EDGE('',*,*,#16432,.F.);
#23478=ORIENTED_EDGE('',*,*,#16434,.T.);
#23479=ORIENTED_EDGE('',*,*,#16431,.F.);
#23480=ORIENTED_EDGE('',*,*,#16435,.T.);
#23481=ORIENTED_EDGE('',*,*,#16436,.T.);
#23482=ORIENTED_EDGE('',*,*,#16435,.F.);
#23483=ORIENTED_EDGE('',*,*,#16434,.F.);
#23484=ORIENTED_EDGE('',*,*,#16433,.T.);
#23485=ORIENTED_EDGE('',*,*,#16430,.F.);
#23486=ORIENTED_EDGE('',*,*,#16437,.F.);
#23487=ORIENTED_EDGE('',*,*,#16438,.F.);
#23488=ORIENTED_EDGE('',*,*,#16439,.F.);
#23489=ORIENTED_EDGE('',*,*,#16440,.F.);
#23490=ORIENTED_EDGE('',*,*,#16441,.F.);
#23491=ORIENTED_EDGE('',*,*,#16442,.F.);
#23492=ORIENTED_EDGE('',*,*,#16426,.T.);
#23493=ORIENTED_EDGE('',*,*,#16436,.F.);
#23494=ORIENTED_EDGE('',*,*,#16437,.T.);
#23495=ORIENTED_EDGE('',*,*,#16443,.F.);
#23496=ORIENTED_EDGE('',*,*,#16444,.F.);
#23497=ORIENTED_EDGE('',*,*,#16445,.T.);
#23498=ORIENTED_EDGE('',*,*,#16438,.T.);
#23499=ORIENTED_EDGE('',*,*,#16445,.F.);
#23500=ORIENTED_EDGE('',*,*,#16446,.F.);
#23501=ORIENTED_EDGE('',*,*,#16447,.T.);
#23502=ORIENTED_EDGE('',*,*,#16439,.T.);
#23503=ORIENTED_EDGE('',*,*,#16447,.F.);
#23504=ORIENTED_EDGE('',*,*,#16448,.F.);
#23505=ORIENTED_EDGE('',*,*,#16449,.T.);
#23506=ORIENTED_EDGE('',*,*,#16440,.T.);
#23507=ORIENTED_EDGE('',*,*,#16449,.F.);
#23508=ORIENTED_EDGE('',*,*,#16450,.F.);
#23509=ORIENTED_EDGE('',*,*,#16451,.T.);
#23510=ORIENTED_EDGE('',*,*,#16441,.T.);
#23511=ORIENTED_EDGE('',*,*,#16451,.F.);
#23512=ORIENTED_EDGE('',*,*,#16452,.F.);
#23513=ORIENTED_EDGE('',*,*,#16453,.T.);
#23514=ORIENTED_EDGE('',*,*,#16442,.T.);
#23515=ORIENTED_EDGE('',*,*,#16453,.F.);
#23516=ORIENTED_EDGE('',*,*,#16454,.F.);
#23517=ORIENTED_EDGE('',*,*,#16443,.T.);
#23518=ORIENTED_EDGE('',*,*,#16444,.T.);
#23519=ORIENTED_EDGE('',*,*,#16454,.T.);
#23520=ORIENTED_EDGE('',*,*,#16452,.T.);
#23521=ORIENTED_EDGE('',*,*,#16450,.T.);
#23522=ORIENTED_EDGE('',*,*,#16448,.T.);
#23523=ORIENTED_EDGE('',*,*,#16446,.T.);
#24201=CYLINDRICAL_SURFACE('',#28565,5.);
#24202=CYLINDRICAL_SURFACE('',#28574,3.);
#25587=ADVANCED_FACE('',(#3634),#24201,.T.);
#25588=ADVANCED_FACE('',(#3635),#576,.T.);
#25589=ADVANCED_FACE('',(#3636),#577,.T.);
#25590=ADVANCED_FACE('',(#3637),#24202,.T.);
#25591=ADVANCED_FACE('',(#3638),#2219,.T.);
#25592=ADVANCED_FACE('',(#3639,#1469),#2220,.T.);
#25593=ADVANCED_FACE('',(#3640,#1470),#2221,.T.);
#25594=ADVANCED_FACE('',(#3641),#2222,.F.);
#25595=ADVANCED_FACE('',(#3642),#2223,.F.);
#25596=ADVANCED_FACE('',(#3643),#2224,.F.);
#25597=ADVANCED_FACE('',(#3644),#2225,.F.);
#25598=ADVANCED_FACE('',(#3645),#2226,.F.);
#25599=ADVANCED_FACE('',(#3646),#2227,.F.);
#25600=ADVANCED_FACE('',(#3647),#2228,.T.);
#25693=CLOSED_SHELL('',(#25587,#25588,#25589,#25590,#25591,#25592,#25593,
#25594,#25595,#25596,#25597,#25598,#25599,#25600));
#28564=AXIS2_PLACEMENT_3D('',#66227,#35680,#35681);
#28565=AXIS2_PLACEMENT_3D('',#66228,#35682,#35683);
#28566=AXIS2_PLACEMENT_3D('',#66230,#35684,#35685);
#28567=AXIS2_PLACEMENT_3D('',#66233,#35687,#35688);
#28568=AXIS2_PLACEMENT_3D('',#66234,#35689,#35690);
#28569=AXIS2_PLACEMENT_3D('',#66237,#35692,#35693);
#28570=AXIS2_PLACEMENT_3D('',#66238,#35694,#35695);
#28571=AXIS2_PLACEMENT_3D('',#66241,#35696,#35697);
#28572=AXIS2_PLACEMENT_3D('',#66244,#35699,#35700);
#28573=AXIS2_PLACEMENT_3D('',#66245,#35701,#35702);
#28574=AXIS2_PLACEMENT_3D('',#66246,#35703,#35704);
#28575=AXIS2_PLACEMENT_3D('',#66249,#35706,#35707);
#28576=AXIS2_PLACEMENT_3D('',#66250,#35708,#35709);
#28577=AXIS2_PLACEMENT_3D('',#66251,#35710,#35711);
#28578=AXIS2_PLACEMENT_3D('',#66264,#35718,#35719);
#28579=AXIS2_PLACEMENT_3D('',#66265,#35720,#35721);
#28580=AXIS2_PLACEMENT_3D('',#66271,#35725,#35726);
#28581=AXIS2_PLACEMENT_3D('',#66275,#35729,#35730);
#28582=AXIS2_PLACEMENT_3D('',#66279,#35733,#35734);
#28583=AXIS2_PLACEMENT_3D('',#66283,#35737,#35738);
#28584=AXIS2_PLACEMENT_3D('',#66287,#35741,#35742);
#28585=AXIS2_PLACEMENT_3D('',#66289,#35744,#35745);
#35680=DIRECTION('axis',(0.,0.,1.));
#35681=DIRECTION('refdir',(1.,0.,0.));
#35682=DIRECTION('center_axis',(1.,1.22464679914735E-16,0.));
#35683=DIRECTION('ref_axis',(-1.22464679914735E-16,1.,0.));
#35684=DIRECTION('center_axis',(1.,1.22464679914735E-16,0.));
#35685=DIRECTION('ref_axis',(-1.22464679914735E-16,1.,0.));
#35686=DIRECTION('',(-1.,-1.22464679914735E-16,0.));
#35687=DIRECTION('center_axis',(1.,1.22464679914735E-16,0.));
#35688=DIRECTION('ref_axis',(-1.22464679914735E-16,1.,0.));
#35689=DIRECTION('center_axis',(1.,1.22464679914735E-16,0.));
#35690=DIRECTION('ref_axis',(-1.22464679914735E-16,1.,0.));
#35691=DIRECTION('',(-0.70710678118655,0.707106781186545,8.6595605623549E-17));
#35692=DIRECTION('center_axis',(1.,1.22464679914735E-16,0.));
#35693=DIRECTION('ref_axis',(-1.22464679914735E-16,1.,0.));
#35694=DIRECTION('center_axis',(-1.,-1.22464679914735E-16,0.));
#35695=DIRECTION('ref_axis',(1.22464679914735E-16,-1.,0.));
#35696=DIRECTION('center_axis',(1.,1.22464679914735E-16,0.));
#35697=DIRECTION('ref_axis',(-1.22464679914735E-16,1.,0.));
#35698=DIRECTION('',(0.707106781186548,-0.707106781186547,8.65956056235493E-17));
#35699=DIRECTION('center_axis',(1.,1.22464679914735E-16,0.));
#35700=DIRECTION('ref_axis',(-1.22464679914735E-16,1.,0.));
#35701=DIRECTION('center_axis',(1.,1.22464679914735E-16,0.));
#35702=DIRECTION('ref_axis',(-1.22464679914735E-16,1.,0.));
#35703=DIRECTION('center_axis',(1.,1.22464679914735E-16,0.));
#35704=DIRECTION('ref_axis',(-1.22464679914735E-16,1.,0.));
#35705=DIRECTION('',(-1.,-1.22464679914735E-16,0.));
#35706=DIRECTION('center_axis',(1.,1.22464679914735E-16,0.));
#35707=DIRECTION('ref_axis',(-1.22464679914735E-16,1.,0.));
#35708=DIRECTION('center_axis',(1.,1.22464679914735E-16,0.));
#35709=DIRECTION('ref_axis',(-1.22464679914735E-16,1.,0.));
#35710=DIRECTION('center_axis',(-1.,-1.22464679914735E-16,0.));
#35711=DIRECTION('ref_axis',(1.22464679914735E-16,-1.,0.));
#35712=DIRECTION('',(0.,0.5,-0.866025403784439));
#35713=DIRECTION('',(0.,1.,0.));
#35714=DIRECTION('',(0.,0.5,0.866025403784439));
#35715=DIRECTION('',(0.,-0.5,0.866025403784438));
#35716=DIRECTION('',(0.,-1.,-1.50231459873716E-16));
#35717=DIRECTION('',(0.,-0.5,-0.866025403784439));
#35718=DIRECTION('center_axis',(1.,1.22464679914735E-16,0.));
#35719=DIRECTION('ref_axis',(-1.22464679914735E-16,1.,0.));
#35720=DIRECTION('center_axis',(-1.06057523872491E-16,0.866025403784439,
0.5));
#35721=DIRECTION('ref_axis',(-5.09861652542584E-33,-0.5,0.866025403784439));
#35722=DIRECTION('',(-1.,-1.22464679914735E-16,0.));
#35723=DIRECTION('',(0.,0.5,-0.866025403784439));
#35724=DIRECTION('',(-1.,-1.22464679914735E-16,0.));
#35725=DIRECTION('center_axis',(0.,0.,1.));
#35726=DIRECTION('ref_axis',(1.,0.,0.));
#35727=DIRECTION('',(0.,1.,0.));
#35728=DIRECTION('',(-1.,-1.22464679914735E-16,0.));
#35729=DIRECTION('center_axis',(1.06057523872491E-16,-0.866025403784439,
0.5));
#35730=DIRECTION('ref_axis',(-8.4117933897259E-34,-0.5,-0.866025403784439));
#35731=DIRECTION('',(0.,0.5,0.866025403784439));
#35732=DIRECTION('',(-1.,-1.22464679914735E-16,0.));
#35733=DIRECTION('center_axis',(1.06057523872491E-16,-0.866025403784439,
-0.5));
#35734=DIRECTION('ref_axis',(-5.93979586439842E-33,0.5,-0.866025403784439));
#35735=DIRECTION('',(0.,-0.5,0.866025403784438));
#35736=DIRECTION('',(-1.,-1.22464679914735E-16,0.));
#35737=DIRECTION('center_axis',(-1.8398047646558E-32,1.50231459873716E-16,
-1.));
#35738=DIRECTION('ref_axis',(0.,1.,1.50231459873716E-16));
#35739=DIRECTION('',(0.,-1.,-1.50231459873716E-16));
#35740=DIRECTION('',(-1.,-1.22464679914735E-16,0.));
#35741=DIRECTION('center_axis',(-1.06057523872491E-16,0.866025403784439,
-0.5));
#35742=DIRECTION('ref_axis',(2.96989793219921E-33,0.5,0.866025403784439));
#35743=DIRECTION('',(0.,-0.5,-0.866025403784439));
#35744=DIRECTION('center_axis',(-1.,0.,0.));
#35745=DIRECTION('ref_axis',(0.,0.,1.));
#66227=CARTESIAN_POINT('',(0.,0.,0.));
#66228=CARTESIAN_POINT('Origin',(20.,1.71450551880629E-15,0.));
#66229=CARTESIAN_POINT('',(0.,-5.,-6.12323399573677E-16));
#66230=CARTESIAN_POINT('Origin',(0.,-7.34788079488412E-16,0.));
#66231=CARTESIAN_POINT('',(-5.4,-5.,-6.12323399573677E-16));
#66232=CARTESIAN_POINT('',(20.,-5.,-6.12323399573677E-16));
#66233=CARTESIAN_POINT('Origin',(-5.4,-1.39609735102798E-15,0.));
#66234=CARTESIAN_POINT('Origin',(-5.4,-1.39609735102798E-15,0.));
#66235=CARTESIAN_POINT('',(-6.,-4.4,-5.38844591624836E-16));
#66236=CARTESIAN_POINT('',(-5.4,-5.,-6.12323399573677E-16));
#66237=CARTESIAN_POINT('Origin',(-6.,-1.46957615897682E-15,0.));
#66238=CARTESIAN_POINT('Origin',(20.,1.71450551880629E-15,0.));
#66239=CARTESIAN_POINT('',(19.4585,-3.,3.67394039744206E-16));
#66240=CARTESIAN_POINT('',(19.4585,3.,-3.67394039744206E-16));
#66241=CARTESIAN_POINT('Origin',(19.4585,1.64819089463247E-15,0.));
#66242=CARTESIAN_POINT('',(20.,2.4585,-3.01079415570377E-16));
#66243=CARTESIAN_POINT('',(20.,2.4585,-3.01079415570377E-16));
#66244=CARTESIAN_POINT('Origin',(20.,1.71450551880629E-15,0.));
#66245=CARTESIAN_POINT('Origin',(19.4585,1.64819089463247E-15,0.));
#66246=CARTESIAN_POINT('Origin',(20.,1.71450551880629E-15,0.));
#66247=CARTESIAN_POINT('',(0.,-3.,-3.67394039744206E-16));
#66248=CARTESIAN_POINT('',(20.,-3.,-3.67394039744206E-16));
#66249=CARTESIAN_POINT('Origin',(0.,-7.34788079488412E-16,0.));
#66250=CARTESIAN_POINT('Origin',(20.,2.4585,0.));
#66251=CARTESIAN_POINT('Origin',(-6.,-1.46957615897682E-15,0.));
#66252=CARTESIAN_POINT('',(-6.,1.44337567297406,2.5));
#66253=CARTESIAN_POINT('',(-6.,2.88675134594813,0.));
#66254=CARTESIAN_POINT('',(-6.,1.44337567297406,2.5));
#66255=CARTESIAN_POINT('',(-6.,-1.44337567297407,2.5));
#66256=CARTESIAN_POINT('',(-6.,-1.44337567297407,2.5));
#66257=CARTESIAN_POINT('',(-6.,-2.88675134594813,-7.77133304087269E-16));
#66258=CARTESIAN_POINT('',(-6.,-2.88675134594813,-7.77133304087269E-16));
#66259=CARTESIAN_POINT('',(-6.,-1.44337567297407,-2.5));
#66260=CARTESIAN_POINT('',(-6.,-1.44337567297407,-2.5));
#66261=CARTESIAN_POINT('',(-6.,1.44337567297406,-2.5));
#66262=CARTESIAN_POINT('',(-6.,1.44337567297406,-2.5));
#66263=CARTESIAN_POINT('',(-6.,2.88675134594813,3.50584097974525E-17));
#66264=CARTESIAN_POINT('Origin',(1.22464679914735E-16,3.,0.));
#66265=CARTESIAN_POINT('Origin',(-3.,1.44337567297406,2.5));
#66266=CARTESIAN_POINT('',(-3.,2.88675134594813,3.50584097974525E-17));
#66267=CARTESIAN_POINT('',(-3.,2.88675134594813,3.50584097974525E-17));
#66268=CARTESIAN_POINT('',(-3.,1.44337567297406,2.5));
#66269=CARTESIAN_POINT('',(-3.,1.44337567297406,2.5));
#66270=CARTESIAN_POINT('',(-3.,1.44337567297406,2.5));
#66271=CARTESIAN_POINT('Origin',(-3.,-1.44337567297407,2.5));
#66272=CARTESIAN_POINT('',(-3.,-1.44337567297407,2.5));
#66273=CARTESIAN_POINT('',(-3.,-1.44337567297407,2.5));
#66274=CARTESIAN_POINT('',(-3.,-1.44337567297407,2.5));
#66275=CARTESIAN_POINT('Origin',(-3.,-2.88675134594813,-7.77133304087269E-16));
#66276=CARTESIAN_POINT('',(-3.,-2.88675134594813,-7.77133304087269E-16));
#66277=CARTESIAN_POINT('',(-3.,-2.88675134594813,-7.77133304087269E-16));
#66278=CARTESIAN_POINT('',(-3.,-2.88675134594813,-7.77133304087269E-16));
#66279=CARTESIAN_POINT('Origin',(-3.,-1.44337567297406,-2.5));
#66280=CARTESIAN_POINT('',(-3.,-1.44337567297406,-2.5));
#66281=CARTESIAN_POINT('',(-3.,-1.44337567297406,-2.5));
#66282=CARTESIAN_POINT('',(-3.,-1.44337567297406,-2.5));
#66283=CARTESIAN_POINT('Origin',(-3.,1.44337567297407,-2.5));
#66284=CARTESIAN_POINT('',(-3.,1.44337567297407,-2.5));
#66285=CARTESIAN_POINT('',(-3.,1.44337567297407,-2.5));
#66286=CARTESIAN_POINT('',(-3.,1.44337567297407,-2.5));
#66287=CARTESIAN_POINT('Origin',(-3.,2.88675134594813,3.50584097974525E-17));
#66288=CARTESIAN_POINT('',(-3.,2.88675134594813,3.50584097974525E-17));
#66289=CARTESIAN_POINT('Origin',(-3.,3.67394039744206E-16,0.));
#66676=UNCERTAINTY_MEASURE_WITH_UNIT(LENGTH_MEASURE(0.01),#66722,
'DISTANCE_ACCURACY_VALUE',
'Maximum model space distance between geometric entities at asserted c
onnectivities');
#66680=UNCERTAINTY_MEASURE_WITH_UNIT(LENGTH_MEASURE(0.01),#66722,
'DISTANCE_ACCURACY_VALUE',
'Maximum model space distance between geometric entities at asserted c
onnectivities');
#66717=(
GEOMETRIC_REPRESENTATION_CONTEXT(3)
GLOBAL_UNCERTAINTY_ASSIGNED_CONTEXT((#66676))
GLOBAL_UNIT_ASSIGNED_CONTEXT((#66722,#66724,#66725))
REPRESENTATION_CONTEXT('','3D')
);
#66721=(
GEOMETRIC_REPRESENTATION_CONTEXT(3)
GLOBAL_UNCERTAINTY_ASSIGNED_CONTEXT((#66680))
GLOBAL_UNIT_ASSIGNED_CONTEXT((#66722,#66724,#66725))
REPRESENTATION_CONTEXT('','3D')
);
#66722=(
LENGTH_UNIT()
NAMED_UNIT(*)
SI_UNIT(.MILLI.,.METRE.)
);
#66724=(
NAMED_UNIT(*)
PLANE_ANGLE_UNIT()
SI_UNIT($,.RADIAN.)
);
#66725=(
NAMED_UNIT(*)
SI_UNIT($,.STERADIAN.)
SOLID_ANGLE_UNIT()
);
#66762=SHAPE_DEFINITION_REPRESENTATION(#66832,#66926);
#66832=PRODUCT_DEFINITION_SHAPE('',$,#66967);
#66926=SHAPE_REPRESENTATION('',(#28564),#66717);
#66930=PRODUCT_DEFINITION_CONTEXT('part definition',#67052,'design');
#66967=PRODUCT_DEFINITION('Socket head cap screw M6x20',
'Socket Head Cap Screw M6x20',#67007,#66930);
#67007=PRODUCT_DEFINITION_FORMATION('',$,#67090);
#67052=APPLICATION_CONTEXT(
'Core Data for Automotive Mechanical Design Process');
#67053=PRODUCT_CONTEXT('part definition',#67052,'mechanical');
#67090=PRODUCT('Socket head cap screw M6x20',
'Socket Head Cap Screw M6x20',$,(#67053));
#67095=PRESENTATION_STYLE_ASSIGNMENT((#67097));
#67097=SURFACE_STYLE_USAGE(.BOTH.,#67099);
#67099=SURFACE_SIDE_STYLE('',(#67101));
#67101=SURFACE_STYLE_FILL_AREA(#67103);
#67103=FILL_AREA_STYLE('Opaque(202,209,238)',(#67105));
#67105=FILL_AREA_STYLE_COLOUR('Opaque(202,209,238)',#67107);
#67107=COLOUR_RGB('Opaque(202,209,238)',0.792156862745098,0.819607843137255,
0.933333333333333);
ENDSEC;
END-ISO-10303-21;
